ISO-10303-21;
HEADER;
/* Generated by software containing ST-Developer
 * from STEP Tools, Inc. (www.steptools.com) 
 */

FILE_DESCRIPTION(
/* description */ ('Rigid flange shaft coupling assembly'),
/* implementation_level */ '2;1');

FILE_NAME(
/* name */ 'Cap Screw - M6x25.step',
/* time_stamp */ '2026-10-27T10:47:16-07:00',
/* author */ (''),
/* organization */ (''),
/* preprocessor_version */ 'ST-DEVELOPER v20.2',
/* originating_system */ 'Autodesk Translation Framework v15.17.0.0',
/* authorisation */ '');

FILE_SCHEMA (('AUTOMOTIVE_DESIGN { 1 0 10303 214 3 1 1 }'));
ENDSEC;

DATA;
#10=MECHANICAL_DESIGN_GEOMETRIC_PRESENTATION_REPRESENTATION('',(#423),#9141);
#30=CONICAL_SURFACE('',#5515,0.475,0.785398163397449);
#31=CONICAL_SURFACE('',#5519,0.485,0.785398163397448);
#32=CONICAL_SURFACE('',#5523,0.31,0.463647609000806);
#33=CONICAL_SURFACE('',#5527,0.27,0.785398163397448);
#40=ORIENTED_CLOSED_SHELL('',*,#4780,.F.);
#43=BREP_WITH_VOIDS('Body1',#4779,(#40));
#366=SHAPE_REPRESENTATION_RELATIONSHIP('SRR','None',#9302,#394);
#394=ADVANCED_BREP_SHAPE_REPRESENTATION('',(#43),#9137);
#423=STYLED_ITEM('',(#9507),#43);
#564=FACE_BOUND('',#1360,.T.);
#714=PLANE('',#5513);
#715=PLANE('',#5521);
#716=PLANE('',#5529);
#717=PLANE('',#5530);
#718=PLANE('',#5531);
#719=PLANE('',#5532);
#720=PLANE('',#5533);
#721=PLANE('',#5534);
#722=PLANE('',#5535);
#723=PLANE('',#5536);
#724=PLANE('',#5537);
#972=FACE_OUTER_BOUND('',#1355,.T.);
#973=FACE_OUTER_BOUND('',#1356,.T.);
#974=FACE_OUTER_BOUND('',#1357,.T.);
#975=FACE_OUTER_BOUND('',#1358,.T.);
#976=FACE_OUTER_BOUND('',#1359,.T.);
#977=FACE_OUTER_BOUND('',#1361,.T.);
#978=FACE_OUTER_BOUND('',#1362,.T.);
#979=FACE_OUTER_BOUND('',#1363,.T.);
#980=FACE_OUTER_BOUND('',#1364,.T.);
#981=FACE_OUTER_BOUND('',#1365,.T.);
#982=FACE_OUTER_BOUND('',#1366,.T.);
#983=FACE_OUTER_BOUND('',#1367,.T.);
#984=FACE_OUTER_BOUND('',#1368,.T.);
#985=FACE_OUTER_BOUND('',#1369,.T.);
#986=FACE_OUTER_BOUND('',#1370,.T.);
#987=FACE_OUTER_BOUND('',#1371,.T.);
#988=FACE_OUTER_BOUND('',#1372,.T.);
#1355=EDGE_LOOP('',(#4223));
#1356=EDGE_LOOP('',(#4224,#4225,#4226,#4227));
#1357=EDGE_LOOP('',(#4228,#4229,#4230,#4231));
#1358=EDGE_LOOP('',(#4232,#4233,#4234,#4235));
#1359=EDGE_LOOP('',(#4236));
#1360=EDGE_LOOP('',(#4237));
#1361=EDGE_LOOP('',(#4238,#4239,#4240,#4241));
#1362=EDGE_LOOP('',(#4242,#4243,#4244,#4245));
#1363=EDGE_LOOP('',(#4246,#4247,#4248,#4249));
#1364=EDGE_LOOP('',(#4250));
#1365=EDGE_LOOP('',(#4251,#4252,#4253,#4254));
#1366=EDGE_LOOP('',(#4255,#4256,#4257,#4258));
#1367=EDGE_LOOP('',(#4259,#4260,#4261,#4262));
#1368=EDGE_LOOP('',(#4263,#4264,#4265,#4266));
#1369=EDGE_LOOP('',(#4267,#4268,#4269,#4270));
#1370=EDGE_LOOP('',(#4271,#4272,#4273,#4274));
#1371=EDGE_LOOP('',(#4275,#4276,#4277,#4278,#4279,#4280));
#1372=EDGE_LOOP('',(#4281,#4282,#4283,#4284,#4285,#4286));
#1694=LINE('',#8805,#2039);
#1695=LINE('',#8809,#2040);
#1696=LINE('',#8813,#2041);
#1697=LINE('',#8820,#2042);
#1698=LINE('',#8824,#2043);
#1699=LINE('',#8828,#2044);
#1700=LINE('',#8833,#2045);
#1701=LINE('',#8835,#2046);
#1702=LINE('',#8837,#2047);
#1703=LINE('',#8838,#2048);
#1704=LINE('',#8841,#2049);
#1705=LINE('',#8843,#2050);
#1706=LINE('',#8844,#2051);
#1707=LINE('',#8847,#2052);
#1708=LINE('',#8849,#2053);
#1709=LINE('',#8850,#2054);
#1710=LINE('',#8853,#2055);
#1711=LINE('',#8855,#2056);
#1712=LINE('',#8856,#2057);
#1713=LINE('',#8859,#2058);
#1714=LINE('',#8861,#2059);
#1715=LINE('',#8862,#2060);
#1716=LINE('',#8864,#2061);
#1717=LINE('',#8865,#2062);
#2039=VECTOR('',#6779,0.475);
#2040=VECTOR('',#6784,0.5);
#2041=VECTOR('',#6789,0.485);
#2042=VECTOR('',#6798,0.31);
#2043=VECTOR('',#6803,0.3);
#2044=VECTOR('',#6808,0.27);
#2045=VECTOR('',#6813,1.);
#2046=VECTOR('',#6814,1.);
#2047=VECTOR('',#6815,1.);
#2048=VECTOR('',#6816,1.);
#2049=VECTOR('',#6819,1.);
#2050=VECTOR('',#6820,1.);
#2051=VECTOR('',#6821,1.);
#2052=VECTOR('',#6824,1.);
#2053=VECTOR('',#6825,1.);
#2054=VECTOR('',#6826,1.);
#2055=VECTOR('',#6829,1.);
#2056=VECTOR('',#6830,1.);
#2057=VECTOR('',#6831,1.);
#2058=VECTOR('',#6834,1.);
#2059=VECTOR('',#6835,1.);
#2060=VECTOR('',#6836,1.);
#2061=VECTOR('',#6839,1.);
#2062=VECTOR('',#6840,1.);
#2256=CIRCLE('',#5514,0.45);
#2257=CIRCLE('',#5516,0.5);
#2258=CIRCLE('',#5518,0.5);
#2259=CIRCLE('',#5520,0.47);
#2260=CIRCLE('',#5522,0.32);
#2261=CIRCLE('',#5524,0.2942);
#2262=CIRCLE('',#5526,0.2942);
#2263=CIRCLE('',#5528,0.24);
#2609=VERTEX_POINT('',#8800);
#2610=VERTEX_POINT('',#8803);
#2611=VERTEX_POINT('',#8807);
#2612=VERTEX_POINT('',#8811);
#2613=VERTEX_POINT('',#8815);
#2614=VERTEX_POINT('',#8818);
#2615=VERTEX_POINT('',#8822);
#2616=VERTEX_POINT('',#8826);
#2617=VERTEX_POINT('',#8831);
#2618=VERTEX_POINT('',#8832);
#2619=VERTEX_POINT('',#8834);
#2620=VERTEX_POINT('',#8836);
#2621=VERTEX_POINT('',#8840);
#2622=VERTEX_POINT('',#8842);
#2623=VERTEX_POINT('',#8846);
#2624=VERTEX_POINT('',#8848);
#2625=VERTEX_POINT('',#8852);
#2626=VERTEX_POINT('',#8854);
#2627=VERTEX_POINT('',#8858);
#2628=VERTEX_POINT('',#8860);
#3155=EDGE_CURVE('',#2609,#2609,#2256,.T.);
#3156=EDGE_CURVE('',#2610,#2610,#2257,.T.);
#3157=EDGE_CURVE('',#2610,#2609,#1694,.T.);
#3158=EDGE_CURVE('',#2611,#2611,#2258,.T.);
#3159=EDGE_CURVE('',#2611,#2610,#1695,.T.);
#3160=EDGE_CURVE('',#2612,#2612,#2259,.T.);
#3161=EDGE_CURVE('',#2612,#2611,#1696,.T.);
#3162=EDGE_CURVE('',#2613,#2613,#2260,.T.);
#3163=EDGE_CURVE('',#2614,#2614,#2261,.F.);
#3164=EDGE_CURVE('',#2614,#2613,#1697,.T.);
#3165=EDGE_CURVE('',#2615,#2615,#2262,.F.);
#3166=EDGE_CURVE('',#2615,#2614,#1698,.T.);
#3167=EDGE_CURVE('',#2616,#2616,#2263,.T.);
#3168=EDGE_CURVE('',#2616,#2615,#1699,.T.);
#3169=EDGE_CURVE('',#2617,#2618,#1700,.T.);
#3170=EDGE_CURVE('',#2618,#2619,#1701,.T.);
#3171=EDGE_CURVE('',#2619,#2620,#1702,.T.);
#3172=EDGE_CURVE('',#2617,#2620,#1703,.T.);
#3173=EDGE_CURVE('',#2618,#2621,#1704,.T.);
#3174=EDGE_CURVE('',#2621,#2622,#1705,.T.);
#3175=EDGE_CURVE('',#2622,#2619,#1706,.T.);
#3176=EDGE_CURVE('',#2621,#2623,#1707,.T.);
#3177=EDGE_CURVE('',#2623,#2624,#1708,.T.);
#3178=EDGE_CURVE('',#2624,#2622,#1709,.T.);
#3179=EDGE_CURVE('',#2623,#2625,#1710,.T.);
#3180=EDGE_CURVE('',#2625,#2626,#1711,.T.);
#3181=EDGE_CURVE('',#2626,#2624,#1712,.T.);
#3182=EDGE_CURVE('',#2625,#2627,#1713,.T.);
#3183=EDGE_CURVE('',#2627,#2628,#1714,.T.);
#3184=EDGE_CURVE('',#2628,#2626,#1715,.T.);
#3185=EDGE_CURVE('',#2627,#2617,#1716,.T.);
#3186=EDGE_CURVE('',#2620,#2628,#1717,.T.);
#4223=ORIENTED_EDGE('',*,*,#3155,.F.);
#4224=ORIENTED_EDGE('',*,*,#3156,.F.);
#4225=ORIENTED_EDGE('',*,*,#3157,.T.);
#4226=ORIENTED_EDGE('',*,*,#3155,.T.);
#4227=ORIENTED_EDGE('',*,*,#3157,.F.);
#4228=ORIENTED_EDGE('',*,*,#3158,.F.);
#4229=ORIENTED_EDGE('',*,*,#3159,.T.);
#4230=ORIENTED_EDGE('',*,*,#3156,.T.);
#4231=ORIENTED_EDGE('',*,*,#3159,.F.);
#4232=ORIENTED_EDGE('',*,*,#3160,.F.);
#4233=ORIENTED_EDGE('',*,*,#3161,.T.);
#4234=ORIENTED_EDGE('',*,*,#3158,.T.);
#4235=ORIENTED_EDGE('',*,*,#3161,.F.);
#4236=ORIENTED_EDGE('',*,*,#3160,.T.);
#4237=ORIENTED_EDGE('',*,*,#3162,.F.);
#4238=ORIENTED_EDGE('',*,*,#3163,.F.);
#4239=ORIENTED_EDGE('',*,*,#3164,.T.);
#4240=ORIENTED_EDGE('',*,*,#3162,.T.);
#4241=ORIENTED_EDGE('',*,*,#3164,.F.);
#4242=ORIENTED_EDGE('',*,*,#3165,.F.);
#4243=ORIENTED_EDGE('',*,*,#3166,.T.);
#4244=ORIENTED_EDGE('',*,*,#3163,.T.);
#4245=ORIENTED_EDGE('',*,*,#3166,.F.);
#4246=ORIENTED_EDGE('',*,*,#3167,.F.);
#4247=ORIENTED_EDGE('',*,*,#3168,.T.);
#4248=ORIENTED_EDGE('',*,*,#3165,.T.);
#4249=ORIENTED_EDGE('',*,*,#3168,.F.);
#4250=ORIENTED_EDGE('',*,*,#3167,.T.);
#4251=ORIENTED_EDGE('',*,*,#3169,.T.);
#4252=ORIENTED_EDGE('',*,*,#3170,.T.);
#4253=ORIENTED_EDGE('',*,*,#3171,.T.);
#4254=ORIENTED_EDGE('',*,*,#3172,.F.);
#4255=ORIENTED_EDGE('',*,*,#3173,.T.);
#4256=ORIENTED_EDGE('',*,*,#3174,.T.);
#4257=ORIENTED_EDGE('',*,*,#3175,.T.);
#4258=ORIENTED_EDGE('',*,*,#3170,.F.);
#4259=ORIENTED_EDGE('',*,*,#3176,.T.);
#4260=ORIENTED_EDGE('',*,*,#3177,.T.);
#4261=ORIENTED_EDGE('',*,*,#3178,.T.);
#4262=ORIENTED_EDGE('',*,*,#3174,.F.);
#4263=ORIENTED_EDGE('',*,*,#3179,.T.);
#4264=ORIENTED_EDGE('',*,*,#3180,.T.);
#4265=ORIENTED_EDGE('',*,*,#3181,.T.);
#4266=ORIENTED_EDGE('',*,*,#3177,.F.);
#4267=ORIENTED_EDGE('',*,*,#3182,.T.);
#4268=ORIENTED_EDGE('',*,*,#3183,.T.);
#4269=ORIENTED_EDGE('',*,*,#3184,.T.);
#4270=ORIENTED_EDGE('',*,*,#3180,.F.);
#4271=ORIENTED_EDGE('',*,*,#3185,.T.);
#4272=ORIENTED_EDGE('',*,*,#3172,.T.);
#4273=ORIENTED_EDGE('',*,*,#3186,.T.);
#4274=ORIENTED_EDGE('',*,*,#3183,.F.);
#4275=ORIENTED_EDGE('',*,*,#3185,.F.);
#4276=ORIENTED_EDGE('',*,*,#3182,.F.);
#4277=ORIENTED_EDGE('',*,*,#3179,.F.);
#4278=ORIENTED_EDGE('',*,*,#3176,.F.);
#4279=ORIENTED_EDGE('',*,*,#3173,.F.);
#4280=ORIENTED_EDGE('',*,*,#3169,.F.);
#4281=ORIENTED_EDGE('',*,*,#3186,.F.);
#4282=ORIENTED_EDGE('',*,*,#3171,.F.);
#4283=ORIENTED_EDGE('',*,*,#3175,.F.);
#4284=ORIENTED_EDGE('',*,*,#3178,.F.);
#4285=ORIENTED_EDGE('',*,*,#3181,.F.);
#4286=ORIENTED_EDGE('',*,*,#3184,.F.);
#4474=CYLINDRICAL_SURFACE('',#5517,0.5);
#4475=CYLINDRICAL_SURFACE('',#5525,0.2942);
#4708=ADVANCED_FACE('',(#972),#714,.T.);
#4709=ADVANCED_FACE('',(#973),#30,.T.);
#4710=ADVANCED_FACE('',(#974),#4474,.T.);
#4711=ADVANCED_FACE('',(#975),#31,.T.);
#4712=ADVANCED_FACE('',(#976,#564),#715,.T.);
#4713=ADVANCED_FACE('',(#977),#32,.T.);
#4714=ADVANCED_FACE('',(#978),#4475,.T.);
#4715=ADVANCED_FACE('',(#979),#33,.T.);
#4716=ADVANCED_FACE('',(#980),#716,.T.);
#4717=ADVANCED_FACE('',(#981),#717,.F.);
#4718=ADVANCED_FACE('',(#982),#718,.F.);
#4719=ADVANCED_FACE('',(#983),#719,.F.);
#4720=ADVANCED_FACE('',(#984),#720,.F.);
#4721=ADVANCED_FACE('',(#985),#721,.F.);
#4722=ADVANCED_FACE('',(#986),#722,.F.);
#4723=ADVANCED_FACE('',(#987),#723,.F.);
#4724=ADVANCED_FACE('',(#988),#724,.F.);
#4779=CLOSED_SHELL('',(#4708,#4709,#4710,#4711,#4712,#4713,#4714,#4715,
#4716));
#4780=CLOSED_SHELL('',(#4717,#4718,#4719,#4720,#4721,#4722,#4723,#4724));
#5512=AXIS2_PLACEMENT_3D('',#8798,#6769,#6770);
#5513=AXIS2_PLACEMENT_3D('',#8799,#6771,#6772);
#5514=AXIS2_PLACEMENT_3D('',#8801,#6773,#6774);
#5515=AXIS2_PLACEMENT_3D('',#8802,#6775,#6776);
#5516=AXIS2_PLACEMENT_3D('',#8804,#6777,#6778);
#5517=AXIS2_PLACEMENT_3D('',#8806,#6780,#6781);
#5518=AXIS2_PLACEMENT_3D('',#8808,#6782,#6783);
#5519=AXIS2_PLACEMENT_3D('',#8810,#6785,#6786);
#5520=AXIS2_PLACEMENT_3D('',#8812,#6787,#6788);
#5521=AXIS2_PLACEMENT_3D('',#8814,#6790,#6791);
#5522=AXIS2_PLACEMENT_3D('',#8816,#6792,#6793);
#5523=AXIS2_PLACEMENT_3D('',#8817,#6794,#6795);
#5524=AXIS2_PLACEMENT_3D('',#8819,#6796,#6797);
#5525=AXIS2_PLACEMENT_3D('',#8821,#6799,#6800);
#5526=AXIS2_PLACEMENT_3D('',#8823,#6801,#6802);
#5527=AXIS2_PLACEMENT_3D('',#8825,#6804,#6805);
#5528=AXIS2_PLACEMENT_3D('',#8827,#6806,#6807);
#5529=AXIS2_PLACEMENT_3D('',#8829,#6809,#6810);
#5530=AXIS2_PLACEMENT_3D('',#8830,#6811,#6812);
#5531=AXIS2_PLACEMENT_3D('',#8839,#6817,#6818);
#5532=AXIS2_PLACEMENT_3D('',#8845,#6822,#6823);
#5533=AXIS2_PLACEMENT_3D('',#8851,#6827,#6828);
#5534=AXIS2_PLACEMENT_3D('',#8857,#6832,#6833);
#5535=AXIS2_PLACEMENT_3D('',#8863,#6837,#6838);
#5536=AXIS2_PLACEMENT_3D('',#8866,#6841,#6842);
#5537=AXIS2_PLACEMENT_3D('',#8867,#6843,#6844);
#6769=DIRECTION('axis',(0.,0.,1.));
#6770=DIRECTION('refdir',(1.,0.,0.));
#6771=DIRECTION('center_axis',(0.,1.,0.));
#6772=DIRECTION('ref_axis',(0.,0.,1.));
#6773=DIRECTION('center_axis',(0.,-1.,0.));
#6774=DIRECTION('ref_axis',(1.,0.,0.));
#6775=DIRECTION('center_axis',(0.,-1.,0.));
#6776=DIRECTION('ref_axis',(1.,0.,0.));
#6777=DIRECTION('center_axis',(0.,-1.,0.));
#6778=DIRECTION('ref_axis',(1.,0.,0.));
#6779=DIRECTION('',(0.707106781186548,0.707106781186547,8.65956056235494E-17));
#6780=DIRECTION('center_axis',(0.,-1.,0.));
#6781=DIRECTION('ref_axis',(1.,0.,0.));
#6782=DIRECTION('center_axis',(0.,-1.,0.));
#6783=DIRECTION('ref_axis',(1.,0.,0.));
#6784=DIRECTION('',(0.,1.,0.));
#6785=DIRECTION('center_axis',(0.,1.,0.));
#6786=DIRECTION('ref_axis',(1.,0.,0.));
#6787=DIRECTION('center_axis',(0.,-1.,0.));
#6788=DIRECTION('ref_axis',(1.,0.,0.));
#6789=DIRECTION('',(-0.707106781186547,0.707106781186548,-8.65956056235493E-17));
#6790=DIRECTION('center_axis',(0.,-1.,0.));
#6791=DIRECTION('ref_axis',(0.,0.,-1.));
#6792=DIRECTION('center_axis',(0.,-1.,0.));
#6793=DIRECTION('ref_axis',(1.,0.,0.));
#6794=DIRECTION('center_axis',(0.,1.,0.));
#6795=DIRECTION('ref_axis',(1.,0.,0.));
#6796=DIRECTION('center_axis',(0.,1.,0.));
#6797=DIRECTION('ref_axis',(1.,0.,0.));
#6798=DIRECTION('',(-0.447213595499958,0.894427190999916,-5.47678698264203E-17));
#6799=DIRECTION('center_axis',(0.,-1.,0.));
#6800=DIRECTION('ref_axis',(1.,0.,0.));
#6801=DIRECTION('center_axis',(0.,1.,0.));
#6802=DIRECTION('ref_axis',(1.,0.,0.));
#6803=DIRECTION('',(0.,1.,0.));
#6804=DIRECTION('center_axis',(0.,1.,0.));
#6805=DIRECTION('ref_axis',(1.,0.,0.));
#6806=DIRECTION('center_axis',(0.,-1.,0.));
#6807=DIRECTION('ref_axis',(1.,0.,0.));
#6808=DIRECTION('',(-0.707106781186547,0.707106781186548,-8.65956056235493E-17));
#6809=DIRECTION('center_axis',(0.,-1.,0.));
#6810=DIRECTION('ref_axis',(0.,0.,-1.));
#6811=DIRECTION('center_axis',(0.866025403784439,0.,-0.5));
#6812=DIRECTION('ref_axis',(0.5,0.,0.866025403784439));
#6813=DIRECTION('',(-0.5,0.,-0.866025403784439));
#6814=DIRECTION('',(0.,-1.,0.));
#6815=DIRECTION('',(0.5,0.,0.866025403784439));
#6816=DIRECTION('',(0.,-1.,0.));
#6817=DIRECTION('center_axis',(1.92296268638356E-16,0.,-1.));
#6818=DIRECTION('ref_axis',(1.,0.,1.92296268638356E-16));
#6819=DIRECTION('',(-1.,0.,-1.92296268638356E-16));
#6820=DIRECTION('',(0.,-1.,0.));
#6821=DIRECTION('',(1.,0.,1.92296268638356E-16));
#6822=DIRECTION('center_axis',(-0.866025403784439,0.,-0.5));
#6823=DIRECTION('ref_axis',(0.5,0.,-0.866025403784439));
#6824=DIRECTION('',(-0.5,0.,0.866025403784438));
#6825=DIRECTION('',(0.,-1.,0.));
#6826=DIRECTION('',(0.5,0.,-0.866025403784438));
#6827=DIRECTION('center_axis',(-0.866025403784439,0.,0.5));
#6828=DIRECTION('ref_axis',(-0.5,0.,-0.866025403784439));
#6829=DIRECTION('',(0.5,0.,0.866025403784439));
#6830=DIRECTION('',(0.,-1.,0.));
#6831=DIRECTION('',(-0.5,0.,-0.866025403784439));
#6832=DIRECTION('center_axis',(-1.92296268638356E-16,0.,1.));
#6833=DIRECTION('ref_axis',(-1.,0.,-1.92296268638356E-16));
#6834=DIRECTION('',(1.,0.,1.92296268638356E-16));
#6835=DIRECTION('',(0.,-1.,0.));
#6836=DIRECTION('',(-1.,0.,-1.92296268638356E-16));
#6837=DIRECTION('center_axis',(0.866025403784439,0.,0.5));
#6838=DIRECTION('ref_axis',(-0.5,0.,0.866025403784439));
#6839=DIRECTION('',(0.5,0.,-0.866025403784439));
#6840=DIRECTION('',(-0.5,0.,0.866025403784439));
#6841=DIRECTION('center_axis',(0.,1.,0.));
#6842=DIRECTION('ref_axis',(1.,0.,0.));
#6843=DIRECTION('center_axis',(0.,-1.,0.));
#6844=DIRECTION('ref_axis',(0.,0.,-1.));
#8798=CARTESIAN_POINT('',(0.,0.,0.));
#8799=CARTESIAN_POINT('Origin',(0.45,0.6,0.));
#8800=CARTESIAN_POINT('',(-0.45,0.6,-5.51091059616309E-17));
#8801=CARTESIAN_POINT('Origin',(0.,0.6,0.));
#8802=CARTESIAN_POINT('Origin',(0.,0.575,0.));
#8803=CARTESIAN_POINT('',(-0.5,0.55,-6.12323399573677E-17));
#8804=CARTESIAN_POINT('Origin',(0.,0.55,0.));
#8805=CARTESIAN_POINT('',(-0.475,0.575,-5.81707229594993E-17));
#8806=CARTESIAN_POINT('Origin',(0.,0.29,0.));
#8807=CARTESIAN_POINT('',(-0.5,0.0299999999999998,-6.12323399573677E-17));
#8808=CARTESIAN_POINT('Origin',(0.,0.0299999999999998,0.));
#8809=CARTESIAN_POINT('',(-0.5,0.29,-6.12323399573677E-17));
#8810=CARTESIAN_POINT('Origin',(0.,0.0150000000000001,0.));
#8811=CARTESIAN_POINT('',(-0.47,7.11236625150491E-17,-5.75583995599256E-17));
#8812=CARTESIAN_POINT('Origin',(0.,0.,0.));
#8813=CARTESIAN_POINT('',(-0.485,0.0150000000000001,-5.93953697586466E-17));
#8814=CARTESIAN_POINT('Origin',(0.32,0.,0.));
#8815=CARTESIAN_POINT('',(-0.32,-6.93889390390723E-18,-3.91886975727153E-17));
#8816=CARTESIAN_POINT('Origin',(0.,0.,0.));
#8817=CARTESIAN_POINT('Origin',(0.,-0.02,0.));
#8818=CARTESIAN_POINT('',(-0.2942,-0.0515999999999999,3.60291088309151E-17));
#8819=CARTESIAN_POINT('Origin',(0.,-0.0515999999999999,0.));
#8820=CARTESIAN_POINT('',(-0.31,-0.02,-3.7964050773568E-17));
#8821=CARTESIAN_POINT('Origin',(0.,-1.24,0.));
#8822=CARTESIAN_POINT('',(-0.2942,-2.4458,3.60291088309151E-17));
#8823=CARTESIAN_POINT('Origin',(0.,-2.4458,0.));
#8824=CARTESIAN_POINT('',(-0.2942,-1.24,-3.60291088309151E-17));
#8825=CARTESIAN_POINT('Origin',(0.,-2.47,0.));
#8826=CARTESIAN_POINT('',(-0.24,-2.5,-2.93915231795365E-17));
#8827=CARTESIAN_POINT('Origin',(0.,-2.5,0.));
#8828=CARTESIAN_POINT('',(-0.27,-2.47,-3.30654635769785E-17));
#8829=CARTESIAN_POINT('Origin',(0.,-2.5,0.));
#8830=CARTESIAN_POINT('Origin',(0.144337567297406,-0.6,-0.25));
#8831=CARTESIAN_POINT('',(0.288675134594813,-0.6,0.));
#8832=CARTESIAN_POINT('',(0.144337567297406,-0.6,-0.25));
#8833=CARTESIAN_POINT('',(0.288675134594813,-0.6,0.));
#8834=CARTESIAN_POINT('',(0.144337567297406,-0.96,-0.25));
#8835=CARTESIAN_POINT('',(0.144337567297406,-0.6,-0.25));
#8836=CARTESIAN_POINT('',(0.288675134594813,-0.96,0.));
#8837=CARTESIAN_POINT('',(0.288675134594813,-0.96,0.));
#8838=CARTESIAN_POINT('',(0.288675134594813,-0.6,0.));
#8839=CARTESIAN_POINT('Origin',(-0.144337567297406,-0.6,-0.25));
#8840=CARTESIAN_POINT('',(-0.144337567297406,-0.6,-0.25));
#8841=CARTESIAN_POINT('',(0.144337567297406,-0.6,-0.25));
#8842=CARTESIAN_POINT('',(-0.144337567297406,-0.96,-0.25));
#8843=CARTESIAN_POINT('',(-0.144337567297406,-0.6,-0.25));
#8844=CARTESIAN_POINT('',(0.144337567297406,-0.96,-0.25));
#8845=CARTESIAN_POINT('Origin',(-0.288675134594813,-0.6,-8.32667268468867E-17));
#8846=CARTESIAN_POINT('',(-0.288675134594813,-0.6,-3.53525079574969E-17));
#8847=CARTESIAN_POINT('',(-0.144337567297406,-0.6,-0.25));
#8848=CARTESIAN_POINT('',(-0.288675134594813,-0.96,-5.55111512312578E-17));
#8849=CARTESIAN_POINT('',(-0.288675134594813,-0.6,-3.53525079574969E-17));
#8850=CARTESIAN_POINT('',(-0.144337567297406,-0.96,-0.25));
#8851=CARTESIAN_POINT('Origin',(-0.144337567297407,-0.6,0.25));
#8852=CARTESIAN_POINT('',(-0.144337567297407,-0.6,0.25));
#8853=CARTESIAN_POINT('',(-0.288675134594813,-0.6,-3.53525079574969E-17));
#8854=CARTESIAN_POINT('',(-0.144337567297407,-0.96,0.25));
#8855=CARTESIAN_POINT('',(-0.144337567297407,-0.6,0.25));
#8856=CARTESIAN_POINT('',(-0.288675134594813,-0.96,-3.53525079574969E-17));
#8857=CARTESIAN_POINT('Origin',(0.144337567297406,-0.6,0.25));
#8858=CARTESIAN_POINT('',(0.144337567297406,-0.6,0.25));
#8859=CARTESIAN_POINT('',(-0.144337567297407,-0.6,0.25));
#8860=CARTESIAN_POINT('',(0.144337567297406,-0.96,0.25));
#8861=CARTESIAN_POINT('',(0.144337567297406,-0.6,0.25));
#8862=CARTESIAN_POINT('',(-0.144337567297407,-0.96,0.25));
#8863=CARTESIAN_POINT('Origin',(0.288675134594813,-0.6,0.));
#8864=CARTESIAN_POINT('',(0.144337567297406,-0.6,0.25));
#8865=CARTESIAN_POINT('',(0.144337567297406,-0.96,0.25));
#8866=CARTESIAN_POINT('Origin',(0.,-0.6,0.));
#8867=CARTESIAN_POINT('Origin',(0.,-0.96,0.));
#9104=UNCERTAINTY_MEASURE_WITH_UNIT(LENGTH_MEASURE(0.001),#9142,
'DISTANCE_ACCURACY_VALUE',
'Maximum model space distance between geometric entities at asserted c
onnectivities');
#9108=UNCERTAINTY_MEASURE_WITH_UNIT(LENGTH_MEASURE(0.001),#9142,
'DISTANCE_ACCURACY_VALUE',
'Maximum model space distance between geometric entities at asserted c
onnectivities');
#9137=(
GEOMETRIC_REPRESENTATION_CONTEXT(3)
GLOBAL_UNCERTAINTY_ASSIGNED_CONTEXT((#9104))
GLOBAL_UNIT_ASSIGNED_CONTEXT((#9142,#9144,#9145))
REPRESENTATION_CONTEXT('','3D')
);
#9141=(
GEOMETRIC_REPRESENTATION_CONTEXT(3)
GLOBAL_UNCERTAINTY_ASSIGNED_CONTEXT((#9108))
GLOBAL_UNIT_ASSIGNED_CONTEXT((#9142,#9144,#9145))
REPRESENTATION_CONTEXT('','3D')
);
#9142=(
LENGTH_UNIT()
NAMED_UNIT(*)
SI_UNIT(.CENTI.,.METRE.)
);
#9144=(
NAMED_UNIT(*)
PLANE_ANGLE_UNIT()
SI_UNIT($,.RADIAN.)
);
#9145=(
NAMED_UNIT(*)
SI_UNIT($,.STERADIAN.)
SOLID_ANGLE_UNIT()
);
#9174=SHAPE_DEFINITION_REPRESENTATION(#9208,#9302);
#9208=PRODUCT_DEFINITION_SHAPE('',$,#9335);
#9302=SHAPE_REPRESENTATION('',(#5512),#9137);
#9306=PRODUCT_DEFINITION_CONTEXT('part definition',#9404,'design');
#9335=PRODUCT_DEFINITION('Cap Screw - M6x25','Cap Screw - M6x25',#9367,
#9306);
#9367=PRODUCT_DEFINITION_FORMATION('',$,#9434);
#9404=APPLICATION_CONTEXT(
'Core Data for Automotive Mechanical Design Process');
#9405=PRODUCT_CONTEXT('part definition',#9404,'mechanical');
#9434=PRODUCT('Cap Screw - M6x25','Cap Screw - M6x25',
'Cap Screw - M6x25',(#9405));
#9501=COLOUR_RGB('Black',0.12,0.14,0.17);
#9502=FILL_AREA_STYLE_COLOUR('',#9501);
#9503=FILL_AREA_STYLE('',(#9502));
#9504=SURFACE_STYLE_FILL_AREA(#9503);
#9505=SURFACE_SIDE_STYLE('',(#9504));
#9506=SURFACE_STYLE_USAGE(.BOTH.,#9505);
#9507=PRESENTATION_STYLE_ASSIGNMENT((#9506));
ENDSEC;
END-ISO-10303-21;
